ISO-10303-21;
HEADER;
FILE_DESCRIPTION((''),'2;1');
FILE_NAME('Pressure Adjusting Screw 3-16 Hex Socket.step','2026-10-06T07:01:46+05:00',(''),(''),'','','');
FILE_SCHEMA (('AUTOMOTIVE_DESIGN { 1 0 10303 214 3 1 1 }'));
ENDSEC;
DATA;
#10=MECHANICAL_DESIGN_GEOMETRIC_PRESENTATION_REPRESENTATION('',(#145),#11396);
#101=CONICAL_SURFACE('',#6278,1.80518500301908,0.785398163397443) ;
#102=CONICAL_SURFACE('',#6282,1.76268064699232,0.75976275487579) ;
#103=CONICAL_SURFACE('',#6286,1.56015989180596,0.67474094222354) ;
#115=SHAPE_REPRESENTATION_RELATIONSHIP('SRR','None',#11462,#130) ;
#130=ADVANCED_BREP_SHAPE_REPRESENTATION('',(#160),#11388) ;
#145=STYLED_ITEM('',(#11546),#160) ;
#160=MANIFOLD_SOLID_BREP('Pressure Adjusting Screw 3-16 Hex Socket',#5576) ;
#367=FACE_BOUND('',#1157,.T.) ;
#479=PLANE('',#6269) ;
#480=PLANE('',#6270) ;
#481=PLANE('',#6271) ;
#482=PLANE('',#6272) ;
#483=PLANE('',#6273) ;
#484=PLANE('',#6274) ;
#485=PLANE('',#6275) ;
#486=PLANE('',#6276) ;
#487=PLANE('',#6288) ;
#783=FACE_OUTER_BOUND('',#1149,.T.) ;
#784=FACE_OUTER_BOUND('',#1150,.T.) ;
#785=FACE_OUTER_BOUND('',#1151,.T.) ;
#786=FACE_OUTER_BOUND('',#1152,.T.) ;
#787=FACE_OUTER_BOUND('',#1153,.T.) ;
#788=FACE_OUTER_BOUND('',#1154,.T.) ;
#789=FACE_OUTER_BOUND('',#1155,.T.) ;
#790=FACE_OUTER_BOUND('',#1156,.T.) ;
#791=FACE_OUTER_BOUND('',#1158,.T.) ;
#792=FACE_OUTER_BOUND('',#1159,.T.) ;
#793=FACE_OUTER_BOUND('',#1160,.T.) ;
#794=FACE_OUTER_BOUND('',#1161,.T.) ;
#795=FACE_OUTER_BOUND('',#1162,.T.) ;
#796=FACE_OUTER_BOUND('',#1163,.T.) ;
#1149=EDGE_LOOP('',(#4826,#4827,#4828,#4829)) ;
#1150=EDGE_LOOP('',(#4830,#4831,#4832,#4833)) ;
#1151=EDGE_LOOP('',(#4834,#4835,#4836,#4837)) ;
#1152=EDGE_LOOP('',(#4838,#4839,#4840,#4841)) ;
#1153=EDGE_LOOP('',(#4842,#4843,#4844,#4845)) ;
#1154=EDGE_LOOP('',(#4846,#4847,#4848,#4849)) ;
#1155=EDGE_LOOP('',(#4850,#4851,#4852,#4853,#4854,#4855)) ;
#1156=EDGE_LOOP('',(#4856)) ;
#1157=EDGE_LOOP('',(#4857,#4858,#4859,#4860,#4861,#4862)) ;
#1158=EDGE_LOOP('',(#4863,#4864,#4865,#4866)) ;
#1159=EDGE_LOOP('',(#4867,#4868,#4869,#4870)) ;
#1160=EDGE_LOOP('',(#4871,#4872,#4873,#4874)) ;
#1161=EDGE_LOOP('',(#4875,#4876,#4877,#4878)) ;
#1162=EDGE_LOOP('',(#4879,#4880,#4881,#4882)) ;
#1163=EDGE_LOOP('',(#4883)) ;
#1534=LINE('',#10927,#1917) ;
#1535=LINE('',#10929,#1918) ;
#1536=LINE('',#10931,#1919) ;
#1537=LINE('',#10932,#1920) ;
#1538=LINE('',#10935,#1921) ;
#1539=LINE('',#10937,#1922) ;
#1540=LINE('',#10938,#1923) ;
#1541=LINE('',#10941,#1924) ;
#1542=LINE('',#10943,#1925) ;
#1543=LINE('',#10944,#1926) ;
#1544=LINE('',#10947,#1927) ;
#1545=LINE('',#10949,#1928) ;
#1546=LINE('',#10950,#1929) ;
#1547=LINE('',#10953,#1930) ;
#1548=LINE('',#10955,#1931) ;
#1549=LINE('',#10956,#1932) ;
#1550=LINE('',#10958,#1933) ;
#1551=LINE('',#10959,#1934) ;
#1552=LINE('',#10967,#1935) ;
#1553=LINE('',#10971,#1936) ;
#1554=LINE('',#10975,#1937) ;
#1555=LINE('',#10979,#1938) ;
#1556=LINE('',#10983,#1939) ;
#1917=VECTOR('',#7768,10.) ;
#1918=VECTOR('',#7769,10.) ;
#1919=VECTOR('',#7770,10.) ;
#1920=VECTOR('',#7771,10.) ;
#1921=VECTOR('',#7774,10.) ;
#1922=VECTOR('',#7775,10.) ;
#1923=VECTOR('',#7776,10.) ;
#1924=VECTOR('',#7779,10.) ;
#1925=VECTOR('',#7780,10.) ;
#1926=VECTOR('',#7781,10.) ;
#1927=VECTOR('',#7784,10.) ;
#1928=VECTOR('',#7785,10.) ;
#1929=VECTOR('',#7786,10.) ;
#1930=VECTOR('',#7789,10.) ;
#1931=VECTOR('',#7790,10.) ;
#1932=VECTOR('',#7791,10.) ;
#1933=VECTOR('',#7794,10.) ;
#1934=VECTOR('',#7795,10.) ;
#1935=VECTOR('',#7806,1.80518500301908) ;
#1936=VECTOR('',#7811,1.90519525249383) ;
#1937=VECTOR('',#7816,1.76268064699232) ;
#1938=VECTOR('',#7821,1.62016604149081) ;
#1939=VECTOR('',#7826,1.56015989180597) ;
#2212=CIRCLE('',#6277,1.70517475354434) ;
#2213=CIRCLE('',#6279,1.90519525249382) ;
#2214=CIRCLE('',#6281,1.90519525249383) ;
#2215=CIRCLE('',#6283,1.62016604149081) ;
#2216=CIRCLE('',#6285,1.62016604149081) ;
#2217=CIRCLE('',#6287,1.50015374212112) ;
#2659=VERTEX_POINT('',#10925) ;
#2660=VERTEX_POINT('',#10926) ;
#2661=VERTEX_POINT('',#10928) ;
#2662=VERTEX_POINT('',#10930) ;
#2663=VERTEX_POINT('',#10934) ;
#2664=VERTEX_POINT('',#10936) ;
#2665=VERTEX_POINT('',#10940) ;
#2666=VERTEX_POINT('',#10942) ;
#2667=VERTEX_POINT('',#10946) ;
#2668=VERTEX_POINT('',#10948) ;
#2669=VERTEX_POINT('',#10952) ;
#2670=VERTEX_POINT('',#10954) ;
#2671=VERTEX_POINT('',#10962) ;
#2672=VERTEX_POINT('',#10965) ;
#2673=VERTEX_POINT('',#10969) ;
#2674=VERTEX_POINT('',#10973) ;
#2675=VERTEX_POINT('',#10977) ;
#2676=VERTEX_POINT('',#10981) ;
#3395=EDGE_CURVE('',#2659,#2660,#1534,.T.) ;
#3396=EDGE_CURVE('',#2659,#2661,#1535,.T.) ;
#3397=EDGE_CURVE('',#2661,#2662,#1536,.T.) ;
#3398=EDGE_CURVE('',#2660,#2662,#1537,.T.) ;
#3399=EDGE_CURVE('',#2660,#2663,#1538,.T.) ;
#3400=EDGE_CURVE('',#2662,#2664,#1539,.T.) ;
#3401=EDGE_CURVE('',#2663,#2664,#1540,.T.) ;
#3402=EDGE_CURVE('',#2663,#2665,#1541,.T.) ;
#3403=EDGE_CURVE('',#2664,#2666,#1542,.T.) ;
#3404=EDGE_CURVE('',#2665,#2666,#1543,.T.) ;
#3405=EDGE_CURVE('',#2665,#2667,#1544,.T.) ;
#3406=EDGE_CURVE('',#2666,#2668,#1545,.T.) ;
#3407=EDGE_CURVE('',#2668,#2667,#1546,.T.) ;
#3408=EDGE_CURVE('',#2669,#2659,#1547,.T.) ;
#3409=EDGE_CURVE('',#2669,#2670,#1548,.T.) ;
#3410=EDGE_CURVE('',#2670,#2661,#1549,.T.) ;
#3411=EDGE_CURVE('',#2667,#2669,#1550,.T.) ;
#3412=EDGE_CURVE('',#2668,#2670,#1551,.T.) ;
#3413=EDGE_CURVE('',#2671,#2671,#2212,.T.) ;
#3414=EDGE_CURVE('',#2672,#2672,#2213,.T.) ;
#3415=EDGE_CURVE('',#2672,#2671,#1552,.T.) ;
#3416=EDGE_CURVE('',#2673,#2673,#2214,.T.) ;
#3417=EDGE_CURVE('',#2673,#2672,#1553,.T.) ;
#3418=EDGE_CURVE('',#2674,#2674,#2215,.T.) ;
#3419=EDGE_CURVE('',#2674,#2673,#1554,.T.) ;
#3420=EDGE_CURVE('',#2675,#2675,#2216,.T.) ;
#3421=EDGE_CURVE('',#2675,#2674,#1555,.T.) ;
#3422=EDGE_CURVE('',#2676,#2676,#2217,.T.) ;
#3423=EDGE_CURVE('',#2676,#2675,#1556,.T.) ;
#4826=ORIENTED_EDGE('',*,*,#3395,.F.) ;
#4827=ORIENTED_EDGE('',*,*,#3396,.T.) ;
#4828=ORIENTED_EDGE('',*,*,#3397,.T.) ;
#4829=ORIENTED_EDGE('',*,*,#3398,.F.) ;
#4830=ORIENTED_EDGE('',*,*,#3399,.F.) ;
#4831=ORIENTED_EDGE('',*,*,#3398,.T.) ;
#4832=ORIENTED_EDGE('',*,*,#3400,.T.) ;
#4833=ORIENTED_EDGE('',*,*,#3401,.F.) ;
#4834=ORIENTED_EDGE('',*,*,#3402,.F.) ;
#4835=ORIENTED_EDGE('',*,*,#3401,.T.) ;
#4836=ORIENTED_EDGE('',*,*,#3403,.T.) ;
#4837=ORIENTED_EDGE('',*,*,#3404,.F.) ;
#4838=ORIENTED_EDGE('',*,*,#3405,.F.) ;
#4839=ORIENTED_EDGE('',*,*,#3404,.T.) ;
#4840=ORIENTED_EDGE('',*,*,#3406,.T.) ;
#4841=ORIENTED_EDGE('',*,*,#3407,.T.) ;
#4842=ORIENTED_EDGE('',*,*,#3408,.F.) ;
#4843=ORIENTED_EDGE('',*,*,#3409,.T.) ;
#4844=ORIENTED_EDGE('',*,*,#3410,.T.) ;
#4845=ORIENTED_EDGE('',*,*,#3396,.F.) ;
#4846=ORIENTED_EDGE('',*,*,#3411,.F.) ;
#4847=ORIENTED_EDGE('',*,*,#3407,.F.) ;
#4848=ORIENTED_EDGE('',*,*,#3412,.T.) ;
#4849=ORIENTED_EDGE('',*,*,#3409,.F.) ;
#4850=ORIENTED_EDGE('',*,*,#3412,.F.) ;
#4851=ORIENTED_EDGE('',*,*,#3406,.F.) ;
#4852=ORIENTED_EDGE('',*,*,#3403,.F.) ;
#4853=ORIENTED_EDGE('',*,*,#3400,.F.) ;
#4854=ORIENTED_EDGE('',*,*,#3397,.F.) ;
#4855=ORIENTED_EDGE('',*,*,#3410,.F.) ;
#4856=ORIENTED_EDGE('',*,*,#3413,.F.) ;
#4857=ORIENTED_EDGE('',*,*,#3405,.T.) ;
#4858=ORIENTED_EDGE('',*,*,#3411,.T.) ;
#4859=ORIENTED_EDGE('',*,*,#3408,.T.) ;
#4860=ORIENTED_EDGE('',*,*,#3395,.T.) ;
#4861=ORIENTED_EDGE('',*,*,#3399,.T.) ;
#4862=ORIENTED_EDGE('',*,*,#3402,.T.) ;
#4863=ORIENTED_EDGE('',*,*,#3414,.F.) ;
#4864=ORIENTED_EDGE('',*,*,#3415,.T.) ;
#4865=ORIENTED_EDGE('',*,*,#3413,.T.) ;
#4866=ORIENTED_EDGE('',*,*,#3415,.F.) ;
#4867=ORIENTED_EDGE('',*,*,#3416,.F.) ;
#4868=ORIENTED_EDGE('',*,*,#3417,.T.) ;
#4869=ORIENTED_EDGE('',*,*,#3414,.T.) ;
#4870=ORIENTED_EDGE('',*,*,#3417,.F.) ;
#4871=ORIENTED_EDGE('',*,*,#3418,.F.) ;
#4872=ORIENTED_EDGE('',*,*,#3419,.T.) ;
#4873=ORIENTED_EDGE('',*,*,#3416,.T.) ;
#4874=ORIENTED_EDGE('',*,*,#3419,.F.) ;
#4875=ORIENTED_EDGE('',*,*,#3420,.F.) ;
#4876=ORIENTED_EDGE('',*,*,#3421,.T.) ;
#4877=ORIENTED_EDGE('',*,*,#3418,.T.) ;
#4878=ORIENTED_EDGE('',*,*,#3421,.F.) ;
#4879=ORIENTED_EDGE('',*,*,#3422,.F.) ;
#4880=ORIENTED_EDGE('',*,*,#3423,.T.) ;
#4881=ORIENTED_EDGE('',*,*,#3420,.T.) ;
#4882=ORIENTED_EDGE('',*,*,#3423,.F.) ;
#4883=ORIENTED_EDGE('',*,*,#3422,.T.) ;
#5210=CYLINDRICAL_SURFACE('',#6280,1.90519525249383) ;
#5211=CYLINDRICAL_SURFACE('',#6284,1.62016604149081) ;
#5508=ADVANCED_FACE('',(#783),#479,.F.) ;
#5509=ADVANCED_FACE('',(#784),#480,.F.) ;
#5510=ADVANCED_FACE('',(#785),#481,.F.) ;
#5511=ADVANCED_FACE('',(#786),#482,.F.) ;
#5512=ADVANCED_FACE('',(#787),#483,.F.) ;
#5513=ADVANCED_FACE('',(#788),#484,.F.) ;
#5514=ADVANCED_FACE('',(#789),#485,.F.) ;
#5515=ADVANCED_FACE('',(#790,#367),#486,.T.) ;
#5516=ADVANCED_FACE('',(#791),#101,.T.) ;
#5517=ADVANCED_FACE('',(#792),#5210,.T.) ;
#5518=ADVANCED_FACE('',(#793),#102,.T.) ;
#5519=ADVANCED_FACE('',(#794),#5211,.T.) ;
#5520=ADVANCED_FACE('',(#795),#103,.T.) ;
#5521=ADVANCED_FACE('',(#796),#487,.T.) ;
#5576=CLOSED_SHELL('',(#5508,#5509,#5510,#5511,#5512,#5513,#5514,#5515,
#5516,#5517,#5518,#5519,#5520,#5521)) ;
#6268=AXIS2_PLACEMENT_3D('',#10923,#7764,#7765) ;
#6269=AXIS2_PLACEMENT_3D('',#10924,#7766,#7767) ;
#6270=AXIS2_PLACEMENT_3D('',#10933,#7772,#7773) ;
#6271=AXIS2_PLACEMENT_3D('',#10939,#7777,#7778) ;
#6272=AXIS2_PLACEMENT_3D('',#10945,#7782,#7783) ;
#6273=AXIS2_PLACEMENT_3D('',#10951,#7787,#7788) ;
#6274=AXIS2_PLACEMENT_3D('',#10957,#7792,#7793) ;
#6275=AXIS2_PLACEMENT_3D('',#10960,#7796,#7797) ;
#6276=AXIS2_PLACEMENT_3D('',#10961,#7798,#7799) ;
#6277=AXIS2_PLACEMENT_3D('',#10963,#7800,#7801) ;
#6278=AXIS2_PLACEMENT_3D('',#10964,#7802,#7803) ;
#6279=AXIS2_PLACEMENT_3D('',#10966,#7804,#7805) ;
#6280=AXIS2_PLACEMENT_3D('',#10968,#7807,#7808) ;
#6281=AXIS2_PLACEMENT_3D('',#10970,#7809,#7810) ;
#6282=AXIS2_PLACEMENT_3D('',#10972,#7812,#7813) ;
#6283=AXIS2_PLACEMENT_3D('',#10974,#7814,#7815) ;
#6284=AXIS2_PLACEMENT_3D('',#10976,#7817,#7818) ;
#6285=AXIS2_PLACEMENT_3D('',#10978,#7819,#7820) ;
#6286=AXIS2_PLACEMENT_3D('',#10980,#7822,#7823) ;
#6287=AXIS2_PLACEMENT_3D('',#10982,#7824,#7825) ;
#6288=AXIS2_PLACEMENT_3D('',#10984,#7827,#7828) ;
#7764=DIRECTION('axis',(0.,0.,1.)) ;
#7765=DIRECTION('refdir',(1.,0.,0.)) ;
#7766=DIRECTION('center_axis',(1.,5.31464800688788E-17,4.4612515253641E-17)) ;
#7767=DIRECTION('ref_axis',(0.,-0.642934102631547,0.76592149706962)) ;
#7768=DIRECTION('',(9.24446373305873E-32,-0.642934102631548,0.765921497069619)) ;
#7769=DIRECTION('',(6.93889390390722E-17,-0.76592149706962,-0.642934102631546)) ;
#7770=DIRECTION('',(2.05699049867507E-32,-0.642934102631547,0.76592149706962)) ;
#7771=DIRECTION('',(6.93889390390722E-17,-0.76592149706962,-0.642934102631546)) ;
#7772=DIRECTION('center_axis',(0.5,-0.55679726583827,0.6633074737669)) ;
#7773=DIRECTION('ref_axis',(-0.866025403784439,-0.321467051315774,0.38296074853481)) ;
#7774=DIRECTION('',(-0.866025403784439,-0.321467051315774,0.38296074853481)) ;
#7775=DIRECTION('',(-0.866025403784438,-0.321467051315774,0.38296074853481)) ;
#7776=DIRECTION('',(6.93889390390722E-17,-0.76592149706962,-0.642934102631546)) ;
#7777=DIRECTION('center_axis',(-0.5,-0.55679726583827,0.6633074737669)) ;
#7778=DIRECTION('ref_axis',(-0.866025403784438,0.321467051315773,-0.38296074853481)) ;
#7779=DIRECTION('',(-0.866025403784439,0.321467051315774,-0.38296074853481)) ;
#7780=DIRECTION('',(-0.866025403784438,0.321467051315773,-0.38296074853481)) ;
#7781=DIRECTION('',(6.93889390390722E-17,-0.76592149706962,-0.642934102631546)) ;
#7782=DIRECTION('center_axis',(-1.,-1.82945775519164E-16,1.10016194411862E-16)) ;
#7783=DIRECTION('ref_axis',(-2.01885846339482E-16,0.642934102631547,-0.76592149706962)) ;
#7784=DIRECTION('',(-2.01885846339482E-16,0.642934102631548,-0.765921497069619)) ;
#7785=DIRECTION('',(-2.01885846339482E-16,0.642934102631547,-0.76592149706962)) ;
#7786=DIRECTION('',(-6.93889390390722E-17,0.76592149706962,0.642934102631546)) ;
#7787=DIRECTION('center_axis',(0.5,0.55679726583827,-0.6633074737669)) ;
#7788=DIRECTION('ref_axis',(0.866025403784439,-0.321467051315773,0.38296074853481)) ;
#7789=DIRECTION('',(0.866025403784439,-0.321467051315774,0.38296074853481)) ;
#7790=DIRECTION('',(6.93889390390722E-17,-0.76592149706962,-0.642934102631546)) ;
#7791=DIRECTION('',(0.866025403784439,-0.321467051315773,0.38296074853481)) ;
#7792=DIRECTION('center_axis',(-0.5,0.55679726583827,-0.6633074737669)) ;
#7793=DIRECTION('ref_axis',(0.866025403784439,0.321467051315774,-0.38296074853481)) ;
#7794=DIRECTION('',(0.866025403784439,0.321467051315774,-0.38296074853481)) ;
#7795=DIRECTION('',(0.866025403784438,0.321467051315774,-0.38296074853481)) ;
#7796=DIRECTION('center_axis',(6.93889390390722E-17,-0.76592149706962,-0.642934102631546)) ;
#7797=DIRECTION('ref_axis',(-1.,0.,-1.07925429301481E-16)) ;
#7798=DIRECTION('center_axis',(0.,0.765921497069619,0.642934102631548)) ;
#7799=DIRECTION('ref_axis',(1.,0.,0.)) ;
#7800=DIRECTION('center_axis',(0.,-0.765921497069619,-0.642934102631548)) ;
#7801=DIRECTION('ref_axis',(1.,0.,0.)) ;
#7802=DIRECTION('center_axis',(0.,-0.765921497069619,-0.642934102631548)) ;
#7803=DIRECTION('ref_axis',(0.,0.642934102631547,-0.76592149706962)) ;
#7804=DIRECTION('center_axis',(0.,-0.765921497069619,-0.642934102631548)) ;
#7805=DIRECTION('ref_axis',(1.,0.,0.)) ;
#7806=DIRECTION('',(8.65956056235489E-17,0.996211348261336,-0.08696522060762)) ;
#7807=DIRECTION('center_axis',(0.,-0.765921497069619,-0.642934102631548)) ;
#7808=DIRECTION('ref_axis',(0.,0.642934102631547,-0.76592149706962)) ;
#7809=DIRECTION('center_axis',(0.,-0.765921497069619,-0.642934102631548)) ;
#7810=DIRECTION('ref_axis',(1.,0.,0.)) ;
#7811=DIRECTION('',(0.,0.765921497069619,0.642934102631548)) ;
#7812=DIRECTION('center_axis',(0.,0.765921497069619,0.642934102631548)) ;
#7813=DIRECTION('ref_axis',(0.,0.642934102631547,-0.76592149706962)) ;
#7814=DIRECTION('center_axis',(0.,-0.765921497069619,-0.642934102631548)) ;
#7815=DIRECTION('ref_axis',(1.,0.,0.)) ;
#7816=DIRECTION('',(-8.43474823948308E-17,0.112472134319156,0.993654879222003)) ;
#7817=DIRECTION('center_axis',(0.,-0.765921497069619,-0.642934102631548)) ;
#7818=DIRECTION('ref_axis',(0.,0.642934102631547,-0.76592149706962)) ;
#7819=DIRECTION('center_axis',(0.,-0.765921497069619,-0.642934102631548)) ;
#7820=DIRECTION('ref_axis',(1.,0.,0.)) ;
#7821=DIRECTION('',(0.,0.765921497069619,0.642934102631548)) ;
#7822=DIRECTION('center_axis',(0.,0.765921497069619,0.642934102631548)) ;
#7823=DIRECTION('ref_axis',(0.,0.642934102631547,-0.76592149706962)) ;
#7824=DIRECTION('center_axis',(0.,-0.765921497069619,-0.642934102631548)) ;
#7825=DIRECTION('ref_axis',(1.,0.,0.)) ;
#7826=DIRECTION('',(-7.65030790430717E-17,0.196446457725814,0.980514553307079)) ;
#7827=DIRECTION('center_axis',(0.,-0.765921497069619,-0.642934102631548)) ;
#7828=DIRECTION('ref_axis',(-1.,0.,0.)) ;
#10923=CARTESIAN_POINT('',(0.,0.,0.)) ;
#10924=CARTESIAN_POINT('Origin',(1.825625,25.3019578297591,32.7334996926975)) ;
#10925=CARTESIAN_POINT('',(1.825625,25.3019578297591,32.7334996926975)) ;
#10926=CARTESIAN_POINT('',(1.825625,24.4180421702409,33.7865003073025)) ;
#10927=CARTESIAN_POINT('',(1.825625,25.6291364148796,32.3437348463488)) ;
#10928=CARTESIAN_POINT('',(1.825625,24.5360363326895,32.090565590066)) ;
#10929=CARTESIAN_POINT('',(1.825625,25.3019578297591,32.7334996926975)) ;
#10930=CARTESIAN_POINT('',(1.825625,23.6521206731713,33.1435662046709)) ;
#10931=CARTESIAN_POINT('',(1.825625,24.5360363326895,32.090565590066)) ;
#10932=CARTESIAN_POINT('',(1.825625,24.4180421702409,33.7865003073025)) ;
#10933=CARTESIAN_POINT('Origin',(1.825625,24.4180421702409,33.7865003073025)) ;
#10934=CARTESIAN_POINT('',(0.635,23.9760843404817,34.3130006146049)) ;
#10935=CARTESIAN_POINT('',(1.89714991361532,24.4445920878011,33.7548716341281)) ;
#10936=CARTESIAN_POINT('',(0.635,23.2101628434121,33.6700665119734)) ;
#10937=CARTESIAN_POINT('',(1.825625,23.6521206731713,33.1435662046709)) ;
#10938=CARTESIAN_POINT('',(0.635,23.9760843404818,34.313000614605)) ;
#10939=CARTESIAN_POINT('Origin',(0.635,23.9760843404818,34.313000614605)) ;
#10940=CARTESIAN_POINT('',(-0.555625,24.4180421702409,33.7865003073025)) ;
#10941=CARTESIAN_POINT('',(-0.0318374136153167,24.2236131729215,34.0181217877793)) ;
#10942=CARTESIAN_POINT('',(-0.555625,23.6521206731713,33.1435662046709)) ;
#10943=CARTESIAN_POINT('',(0.635,23.2101628434121,33.6700665119734)) ;
#10944=CARTESIAN_POINT('',(-0.555625,24.4180421702409,33.7865003073025)) ;
#10945=CARTESIAN_POINT('Origin',(-0.555625,24.4180421702409,33.7865003073025)) ;
#10946=CARTESIAN_POINT('',(-0.555625,25.3019578297591,32.7334996926975)) ;
#10947=CARTESIAN_POINT('',(-0.555625,25.1871785851204,32.8702351536512)) ;
#10948=CARTESIAN_POINT('',(-0.555625,24.5360363326895,32.090565590066)) ;
#10949=CARTESIAN_POINT('',(-0.555625,23.6521206731713,33.1435662046709)) ;
#10950=CARTESIAN_POINT('',(-0.555625,25.3019578297591,32.7334996926975)) ;
#10951=CARTESIAN_POINT('Origin',(0.635,25.7439156595183,32.2069993853951)) ;
#10952=CARTESIAN_POINT('',(0.635,25.7439156595183,32.206999385395)) ;
#10953=CARTESIAN_POINT('',(0.563475086384684,25.7704655770785,32.1753707122207)) ;
#10954=CARTESIAN_POINT('',(0.635,24.9779941624486,31.5640652827635)) ;
#10955=CARTESIAN_POINT('',(0.635,25.7439156595183,32.2069993853951)) ;
#10956=CARTESIAN_POINT('',(0.635,24.9779941624486,31.5640652827635)) ;
#10957=CARTESIAN_POINT('Origin',(-0.555625,25.3019578297591,32.7334996926975)) ;
#10958=CARTESIAN_POINT('',(0.111212413615316,25.5494866621989,32.4386208658719)) ;
#10959=CARTESIAN_POINT('',(-0.555625,24.5360363326895,32.090565590066)) ;
#10960=CARTESIAN_POINT('Origin',(0.635,24.0940785029304,32.6170658973685)) ;
#10961=CARTESIAN_POINT('Origin',(0.635,25.956315,31.95397)) ;
#10962=CARTESIAN_POINT('',(0.635,23.763685,34.56603)) ;
#10963=CARTESIAN_POINT('Origin',(0.635,24.86,33.26)) ;
#10964=CARTESIAN_POINT('Origin',(0.635,24.7834,33.1957)) ;
#10965=CARTESIAN_POINT('',(0.635,23.481885,34.59063)) ;
#10966=CARTESIAN_POINT('Origin',(0.635,24.7068,33.1314)) ;
#10967=CARTESIAN_POINT('',(0.635,23.622785,34.57833)) ;
#10968=CARTESIAN_POINT('Origin',(0.635,23.260975,31.9177375)) ;
#10969=CARTESIAN_POINT('',(0.635,20.590235,32.163305)) ;
#10970=CARTESIAN_POINT('Origin',(0.635,21.81515,30.704075)) ;
#10971=CARTESIAN_POINT('',(0.635,22.03606,33.3769675)) ;
#10972=CARTESIAN_POINT('Origin',(0.635,21.70025,30.607625)) ;
#10973=CARTESIAN_POINT('',(0.635,20.54369,31.752095)) ;
#10974=CARTESIAN_POINT('Origin',(0.635,21.58535,30.511175)) ;
#10975=CARTESIAN_POINT('',(0.635,20.5669625,31.9577)) ;
#10976=CARTESIAN_POINT('Origin',(0.635,21.16405,30.157525)) ;
#10977=CARTESIAN_POINT('',(0.635,19.70109,31.044795)) ;
#10978=CARTESIAN_POINT('Origin',(0.635,20.74275,29.803875)) ;
#10979=CARTESIAN_POINT('',(0.635,20.12239,31.398445)) ;
#10980=CARTESIAN_POINT('Origin',(0.635,20.6853,29.75565)) ;
#10981=CARTESIAN_POINT('',(0.635,19.66335,30.856425)) ;
#10982=CARTESIAN_POINT('Origin',(0.635,20.62785,29.707425)) ;
#10983=CARTESIAN_POINT('',(0.635,19.68222,30.95061)) ;
#10984=CARTESIAN_POINT('Origin',(0.635,20.62785,29.707425)) ;
#11371=UNCERTAINTY_MEASURE_WITH_UNIT(LENGTH_MEASURE(0.01),#11397,
'DISTANCE_ACCURACY_VALUE',
'Maximum model space distance between geometric entities at asserted c
onnectivities') ;
#11379=UNCERTAINTY_MEASURE_WITH_UNIT(LENGTH_MEASURE(0.01),#11397,
'DISTANCE_ACCURACY_VALUE',
'Maximum model space distance between geometric entities at asserted c
onnectivities') ;
#11388=(
GEOMETRIC_REPRESENTATION_CONTEXT(3)
GLOBAL_UNCERTAINTY_ASSIGNED_CONTEXT((#11371))
GLOBAL_UNIT_ASSIGNED_CONTEXT((#11397,#11399,#11400))
REPRESENTATION_CONTEXT('','3D')
) ;
#11396=(
GEOMETRIC_REPRESENTATION_CONTEXT(3)
GLOBAL_UNCERTAINTY_ASSIGNED_CONTEXT((#11379))
GLOBAL_UNIT_ASSIGNED_CONTEXT((#11397,#11399,#11400))
REPRESENTATION_CONTEXT('','3D')
) ;
#11397=(
LENGTH_UNIT()
NAMED_UNIT(*)
SI_UNIT(.MILLI.,.METRE.)
) ;
#11399=(
NAMED_UNIT(*)
PLANE_ANGLE_UNIT()
SI_UNIT($,.RADIAN.)
) ;
#11400=(
NAMED_UNIT(*)
SI_UNIT($,.STERADIAN.)
SOLID_ANGLE_UNIT()
) ;
#11409=SHAPE_DEFINITION_REPRESENTATION(#11425,#11462) ;
#11425=PRODUCT_DEFINITION_SHAPE('',$,#11479) ;
#11462=SHAPE_REPRESENTATION('',(#6268),#11388) ;
#11470=PRODUCT_DEFINITION_CONTEXT('part definition',#11520,'design') ;
#11479=PRODUCT_DEFINITION('Pressure Adjusting Screw 3-16 Hex Socket',
'Pressure Adjusting Screw 3-16 Hex Socket',#11495,#11470) ;
#11495=PRODUCT_DEFINITION_FORMATION('',$,#11530) ;
#11520=APPLICATION_CONTEXT(
'Core Data for Automotive Mechanical Design Process') ;
#11521=PRODUCT_CONTEXT('part definition',#11520,'mechanical') ;
#11530=PRODUCT('Pressure Adjusting Screw 3-16 Hex Socket',
'Pressure Adjusting Screw 3-16 Hex Socket',$,(#11521)) ;
#11546=PRESENTATION_STYLE_ASSIGNMENT((#11562)) ;
#11562=SURFACE_STYLE_USAGE(.BOTH.,#11578) ;
#11578=SURFACE_SIDE_STYLE('',(#11594)) ;
#11594=SURFACE_STYLE_FILL_AREA(#11610) ;
#11610=FILL_AREA_STYLE(
'MAS-252 Metallic - Pressure Adjusting Screw 3-16 Hex Socket',(#11626)) ;
#11626=FILL_AREA_STYLE_COLOUR(
'MAS-252 Metallic - Pressure Adjusting Screw 3-16 Hex Socket',#11642) ;
#11642=COLOUR_RGB(
'MAS-252 Metallic - Pressure Adjusting Screw 3-16 Hex Socket', 0.66274510, 0.83137255, 0.94901961) ;
ENDSEC;
END-ISO-10303-21;
